ISO-10303-21;
HEADER;
/* Generated by software containing ST-Developer
 * from STEP Tools, Inc. (www.steptools.com) 
 */

FILE_DESCRIPTION(
/* description */ ('Belt tension measurement rig'),
/* implementation_level */ '2;1');

FILE_NAME(
/* name */ 'Screw support (1).step',
/* time_stamp */ '2026-10-28T03:24:44-07:00',
/* author */ (''),
/* organization */ (''),
/* preprocessor_version */ 'ST-DEVELOPER v20.2',
/* originating_system */ 'Autodesk Translation Framework v15.17.0.0',
/* authorisation */ '');

FILE_SCHEMA (('AUTOMOTIVE_DESIGN { 1 0 10303 214 3 1 1 }'));
ENDSEC;

DATA;
#10=MECHANICAL_DESIGN_GEOMETRIC_PRESENTATION_REPRESENTATION('',(#701),#23587);
#591=SHAPE_REPRESENTATION_RELATIONSHIP('SRR','None',#23836,#646);
#646=ADVANCED_BREP_SHAPE_REPRESENTATION('',(#771),#23534);
#701=STYLED_ITEM('',(#24218),#771);
#771=MANIFOLD_SOLID_BREP('Body1',#12206);
#879=FACE_BOUND('',#2220,.T.);
#880=FACE_BOUND('',#2223,.T.);
#881=FACE_BOUND('',#2229,.T.);
#882=FACE_BOUND('',#2232,.T.);
#883=FACE_BOUND('',#2234,.T.);
#884=FACE_BOUND('',#2235,.T.);
#885=FACE_BOUND('',#2237,.T.);
#886=FACE_BOUND('',#2238,.T.);
#1097=PLANE('',#13107);
#1098=PLANE('',#13112);
#1099=PLANE('',#13121);
#1100=PLANE('',#13122);
#1101=PLANE('',#13123);
#1102=PLANE('',#13124);
#1103=PLANE('',#13125);
#1104=PLANE('',#13126);
#1464=FACE_OUTER_BOUND('',#2218,.T.);
#1465=FACE_OUTER_BOUND('',#2219,.T.);
#1466=FACE_OUTER_BOUND('',#2221,.T.);
#1467=FACE_OUTER_BOUND('',#2222,.T.);
#1468=FACE_OUTER_BOUND('',#2224,.T.);
#1469=FACE_OUTER_BOUND('',#2225,.T.);
#1470=FACE_OUTER_BOUND('',#2226,.T.);
#1471=FACE_OUTER_BOUND('',#2227,.T.);
#1472=FACE_OUTER_BOUND('',#2228,.T.);
#1473=FACE_OUTER_BOUND('',#2230,.T.);
#1474=FACE_OUTER_BOUND('',#2231,.T.);
#1475=FACE_OUTER_BOUND('',#2233,.T.);
#1476=FACE_OUTER_BOUND('',#2236,.T.);
#2218=EDGE_LOOP('',(#8394,#8395,#8396,#8397));
#2219=EDGE_LOOP('',(#8398));
#2220=EDGE_LOOP('',(#8399));
#2221=EDGE_LOOP('',(#8400,#8401,#8402,#8403));
#2222=EDGE_LOOP('',(#8404));
#2223=EDGE_LOOP('',(#8405));
#2224=EDGE_LOOP('',(#8406,#8407,#8408,#8409));
#2225=EDGE_LOOP('',(#8410,#8411,#8412,#8413));
#2226=EDGE_LOOP('',(#8414,#8415,#8416,#8417));
#2227=EDGE_LOOP('',(#8418,#8419,#8420,#8421));
#2228=EDGE_LOOP('',(#8422,#8423,#8424,#8425));
#2229=EDGE_LOOP('',(#8426));
#2230=EDGE_LOOP('',(#8427,#8428,#8429,#8430));
#2231=EDGE_LOOP('',(#8431,#8432,#8433,#8434));
#2232=EDGE_LOOP('',(#8435));
#2233=EDGE_LOOP('',(#8436,#8437,#8438,#8439));
#2234=EDGE_LOOP('',(#8440));
#2235=EDGE_LOOP('',(#8441));
#2236=EDGE_LOOP('',(#8442,#8443,#8444,#8445));
#2237=EDGE_LOOP('',(#8446));
#2238=EDGE_LOOP('',(#8447));
#3092=LINE('',#19058,#3843);
#3093=LINE('',#19067,#3844);
#3094=LINE('',#19075,#3845);
#3095=LINE('',#19079,#3846);
#3096=LINE('',#19084,#3847);
#3097=LINE('',#19089,#3848);
#3098=LINE('',#19091,#3849);
#3099=LINE('',#19093,#3850);
#3100=LINE('',#19094,#3851);
#3101=LINE('',#19097,#3852);
#3102=LINE('',#19099,#3853);
#3103=LINE('',#19100,#3854);
#3104=LINE('',#19103,#3855);
#3105=LINE('',#19105,#3856);
#3106=LINE('',#19106,#3857);
#3107=LINE('',#19108,#3858);
#3108=LINE('',#19109,#3859);
#3843=VECTOR('',#15101,0.399999999999999);
#3844=VECTOR('',#15112,0.399999999999999);
#3845=VECTOR('',#15123,0.225000000000001);
#3846=VECTOR('',#15128,0.225000000000001);
#3847=VECTOR('',#15133,0.8);
#3848=VECTOR('',#15138,1.);
#3849=VECTOR('',#15139,1.);
#3850=VECTOR('',#15140,1.);
#3851=VECTOR('',#15141,1.);
#3852=VECTOR('',#15144,1.);
#3853=VECTOR('',#15145,1.);
#3854=VECTOR('',#15146,1.);
#3855=VECTOR('',#15149,1.);
#3856=VECTOR('',#15150,1.);
#3857=VECTOR('',#15151,1.);
#3858=VECTOR('',#15154,1.);
#3859=VECTOR('',#15155,1.);
#4574=CIRCLE('',#13105,0.399999999999999);
#4575=CIRCLE('',#13106,0.399999999999999);
#4576=CIRCLE('',#13108,0.225000000000001);
#4577=CIRCLE('',#13110,0.399999999999999);
#4578=CIRCLE('',#13111,0.399999999999999);
#4579=CIRCLE('',#13113,0.225000000000001);
#4580=CIRCLE('',#13115,0.225000000000001);
#4581=CIRCLE('',#13117,0.225000000000001);
#4582=CIRCLE('',#13119,0.8);
#4583=CIRCLE('',#13120,0.8);
#5390=VERTEX_POINT('',#19055);
#5391=VERTEX_POINT('',#19057);
#5392=VERTEX_POINT('',#19061);
#5393=VERTEX_POINT('',#19064);
#5394=VERTEX_POINT('',#19066);
#5395=VERTEX_POINT('',#19070);
#5396=VERTEX_POINT('',#19073);
#5397=VERTEX_POINT('',#19077);
#5398=VERTEX_POINT('',#19081);
#5399=VERTEX_POINT('',#19083);
#5400=VERTEX_POINT('',#19087);
#5401=VERTEX_POINT('',#19088);
#5402=VERTEX_POINT('',#19090);
#5403=VERTEX_POINT('',#19092);
#5404=VERTEX_POINT('',#19096);
#5405=VERTEX_POINT('',#19098);
#5406=VERTEX_POINT('',#19102);
#5407=VERTEX_POINT('',#19104);
#6556=EDGE_CURVE('',#5390,#5390,#4574,.T.);
#6557=EDGE_CURVE('',#5390,#5391,#3092,.T.);
#6558=EDGE_CURVE('',#5391,#5391,#4575,.T.);
#6559=EDGE_CURVE('',#5392,#5392,#4576,.T.);
#6560=EDGE_CURVE('',#5393,#5393,#4577,.T.);
#6561=EDGE_CURVE('',#5393,#5394,#3093,.T.);
#6562=EDGE_CURVE('',#5394,#5394,#4578,.T.);
#6563=EDGE_CURVE('',#5395,#5395,#4579,.T.);
#6564=EDGE_CURVE('',#5396,#5396,#4580,.T.);
#6565=EDGE_CURVE('',#5396,#5392,#3094,.T.);
#6566=EDGE_CURVE('',#5397,#5397,#4581,.T.);
#6567=EDGE_CURVE('',#5397,#5395,#3095,.T.);
#6568=EDGE_CURVE('',#5398,#5398,#4582,.T.);
#6569=EDGE_CURVE('',#5398,#5399,#3096,.T.);
#6570=EDGE_CURVE('',#5399,#5399,#4583,.T.);
#6571=EDGE_CURVE('',#5400,#5401,#3097,.T.);
#6572=EDGE_CURVE('',#5401,#5402,#3098,.T.);
#6573=EDGE_CURVE('',#5403,#5402,#3099,.T.);
#6574=EDGE_CURVE('',#5400,#5403,#3100,.T.);
#6575=EDGE_CURVE('',#5404,#5400,#3101,.T.);
#6576=EDGE_CURVE('',#5405,#5403,#3102,.T.);
#6577=EDGE_CURVE('',#5404,#5405,#3103,.T.);
#6578=EDGE_CURVE('',#5406,#5404,#3104,.T.);
#6579=EDGE_CURVE('',#5407,#5405,#3105,.T.);
#6580=EDGE_CURVE('',#5406,#5407,#3106,.T.);
#6581=EDGE_CURVE('',#5401,#5406,#3107,.T.);
#6582=EDGE_CURVE('',#5402,#5407,#3108,.T.);
#8394=ORIENTED_EDGE('',*,*,#6556,.F.);
#8395=ORIENTED_EDGE('',*,*,#6557,.T.);
#8396=ORIENTED_EDGE('',*,*,#6558,.F.);
#8397=ORIENTED_EDGE('',*,*,#6557,.F.);
#8398=ORIENTED_EDGE('',*,*,#6556,.T.);
#8399=ORIENTED_EDGE('',*,*,#6559,.F.);
#8400=ORIENTED_EDGE('',*,*,#6560,.F.);
#8401=ORIENTED_EDGE('',*,*,#6561,.T.);
#8402=ORIENTED_EDGE('',*,*,#6562,.F.);
#8403=ORIENTED_EDGE('',*,*,#6561,.F.);
#8404=ORIENTED_EDGE('',*,*,#6560,.T.);
#8405=ORIENTED_EDGE('',*,*,#6563,.F.);
#8406=ORIENTED_EDGE('',*,*,#6564,.F.);
#8407=ORIENTED_EDGE('',*,*,#6565,.T.);
#8408=ORIENTED_EDGE('',*,*,#6559,.T.);
#8409=ORIENTED_EDGE('',*,*,#6565,.F.);
#8410=ORIENTED_EDGE('',*,*,#6566,.F.);
#8411=ORIENTED_EDGE('',*,*,#6567,.T.);
#8412=ORIENTED_EDGE('',*,*,#6563,.T.);
#8413=ORIENTED_EDGE('',*,*,#6567,.F.);
#8414=ORIENTED_EDGE('',*,*,#6568,.F.);
#8415=ORIENTED_EDGE('',*,*,#6569,.T.);
#8416=ORIENTED_EDGE('',*,*,#6570,.F.);
#8417=ORIENTED_EDGE('',*,*,#6569,.F.);
#8418=ORIENTED_EDGE('',*,*,#6571,.T.);
#8419=ORIENTED_EDGE('',*,*,#6572,.T.);
#8420=ORIENTED_EDGE('',*,*,#6573,.F.);
#8421=ORIENTED_EDGE('',*,*,#6574,.F.);
#8422=ORIENTED_EDGE('',*,*,#6575,.T.);
#8423=ORIENTED_EDGE('',*,*,#6574,.T.);
#8424=ORIENTED_EDGE('',*,*,#6576,.F.);
#8425=ORIENTED_EDGE('',*,*,#6577,.F.);
#8426=ORIENTED_EDGE('',*,*,#6570,.T.);
#8427=ORIENTED_EDGE('',*,*,#6578,.T.);
#8428=ORIENTED_EDGE('',*,*,#6577,.T.);
#8429=ORIENTED_EDGE('',*,*,#6579,.F.);
#8430=ORIENTED_EDGE('',*,*,#6580,.F.);
#8431=ORIENTED_EDGE('',*,*,#6581,.T.);
#8432=ORIENTED_EDGE('',*,*,#6580,.T.);
#8433=ORIENTED_EDGE('',*,*,#6582,.F.);
#8434=ORIENTED_EDGE('',*,*,#6572,.F.);
#8435=ORIENTED_EDGE('',*,*,#6568,.T.);
#8436=ORIENTED_EDGE('',*,*,#6582,.T.);
#8437=ORIENTED_EDGE('',*,*,#6579,.T.);
#8438=ORIENTED_EDGE('',*,*,#6576,.T.);
#8439=ORIENTED_EDGE('',*,*,#6573,.T.);
#8440=ORIENTED_EDGE('',*,*,#6558,.T.);
#8441=ORIENTED_EDGE('',*,*,#6562,.T.);
#8442=ORIENTED_EDGE('',*,*,#6581,.F.);
#8443=ORIENTED_EDGE('',*,*,#6571,.F.);
#8444=ORIENTED_EDGE('',*,*,#6575,.F.);
#8445=ORIENTED_EDGE('',*,*,#6578,.F.);
#8446=ORIENTED_EDGE('',*,*,#6564,.T.);
#8447=ORIENTED_EDGE('',*,*,#6566,.T.);
#11210=CYLINDRICAL_SURFACE('',#13104,0.399999999999999);
#11211=CYLINDRICAL_SURFACE('',#13109,0.399999999999999);
#11212=CYLINDRICAL_SURFACE('',#13114,0.225000000000001);
#11213=CYLINDRICAL_SURFACE('',#13116,0.225000000000001);
#11214=CYLINDRICAL_SURFACE('',#13118,0.8);
#11605=ADVANCED_FACE('',(#1464),#11210,.F.);
#11606=ADVANCED_FACE('',(#1465,#879),#1097,.T.);
#11607=ADVANCED_FACE('',(#1466),#11211,.F.);
#11608=ADVANCED_FACE('',(#1467,#880),#1098,.T.);
#11609=ADVANCED_FACE('',(#1468),#11212,.F.);
#11610=ADVANCED_FACE('',(#1469),#11213,.F.);
#11611=ADVANCED_FACE('',(#1470),#11214,.F.);
#11612=ADVANCED_FACE('',(#1471),#1099,.T.);
#11613=ADVANCED_FACE('',(#1472,#881),#1100,.T.);
#11614=ADVANCED_FACE('',(#1473),#1101,.T.);
#11615=ADVANCED_FACE('',(#1474,#882),#1102,.T.);
#11616=ADVANCED_FACE('',(#1475,#883,#884),#1103,.T.);
#11617=ADVANCED_FACE('',(#1476,#885,#886),#1104,.F.);
#12206=CLOSED_SHELL('',(#11605,#11606,#11607,#11608,#11609,#11610,#11611,
#11612,#11613,#11614,#11615,#11616,#11617));
#13103=AXIS2_PLACEMENT_3D('',#19053,#15095,#15096);
#13104=AXIS2_PLACEMENT_3D('',#19054,#15097,#15098);
#13105=AXIS2_PLACEMENT_3D('',#19056,#15099,#15100);
#13106=AXIS2_PLACEMENT_3D('',#19059,#15102,#15103);
#13107=AXIS2_PLACEMENT_3D('',#19060,#15104,#15105);
#13108=AXIS2_PLACEMENT_3D('',#19062,#15106,#15107);
#13109=AXIS2_PLACEMENT_3D('',#19063,#15108,#15109);
#13110=AXIS2_PLACEMENT_3D('',#19065,#15110,#15111);
#13111=AXIS2_PLACEMENT_3D('',#19068,#15113,#15114);
#13112=AXIS2_PLACEMENT_3D('',#19069,#15115,#15116);
#13113=AXIS2_PLACEMENT_3D('',#19071,#15117,#15118);
#13114=AXIS2_PLACEMENT_3D('',#19072,#15119,#15120);
#13115=AXIS2_PLACEMENT_3D('',#19074,#15121,#15122);
#13116=AXIS2_PLACEMENT_3D('',#19076,#15124,#15125);
#13117=AXIS2_PLACEMENT_3D('',#19078,#15126,#15127);
#13118=AXIS2_PLACEMENT_3D('',#19080,#15129,#15130);
#13119=AXIS2_PLACEMENT_3D('',#19082,#15131,#15132);
#13120=AXIS2_PLACEMENT_3D('',#19085,#15134,#15135);
#13121=AXIS2_PLACEMENT_3D('',#19086,#15136,#15137);
#13122=AXIS2_PLACEMENT_3D('',#19095,#15142,#15143);
#13123=AXIS2_PLACEMENT_3D('',#19101,#15147,#15148);
#13124=AXIS2_PLACEMENT_3D('',#19107,#15152,#15153);
#13125=AXIS2_PLACEMENT_3D('',#19110,#15156,#15157);
#13126=AXIS2_PLACEMENT_3D('',#19111,#15158,#15159);
#15095=DIRECTION('axis',(0.,0.,1.));
#15096=DIRECTION('refdir',(1.,0.,0.));
#15097=DIRECTION('center_axis',(0.,0.,1.));
#15098=DIRECTION('ref_axis',(1.,0.,0.));
#15099=DIRECTION('center_axis',(0.,0.,1.));
#15100=DIRECTION('ref_axis',(1.,0.,0.));
#15101=DIRECTION('',(0.,0.,1.));
#15102=DIRECTION('center_axis',(0.,0.,-1.));
#15103=DIRECTION('ref_axis',(1.,0.,0.));
#15104=DIRECTION('center_axis',(0.,0.,1.));
#15105=DIRECTION('ref_axis',(1.,0.,0.));
#15106=DIRECTION('center_axis',(0.,0.,1.));
#15107=DIRECTION('ref_axis',(1.,0.,0.));
#15108=DIRECTION('center_axis',(0.,0.,1.));
#15109=DIRECTION('ref_axis',(1.,0.,0.));
#15110=DIRECTION('center_axis',(0.,0.,1.));
#15111=DIRECTION('ref_axis',(1.,0.,0.));
#15112=DIRECTION('',(0.,0.,1.));
#15113=DIRECTION('center_axis',(0.,0.,-1.));
#15114=DIRECTION('ref_axis',(1.,0.,0.));
#15115=DIRECTION('center_axis',(0.,0.,1.));
#15116=DIRECTION('ref_axis',(1.,0.,0.));
#15117=DIRECTION('center_axis',(0.,0.,1.));
#15118=DIRECTION('ref_axis',(1.,0.,0.));
#15119=DIRECTION('center_axis',(0.,0.,1.));
#15120=DIRECTION('ref_axis',(1.,0.,0.));
#15121=DIRECTION('center_axis',(0.,0.,1.));
#15122=DIRECTION('ref_axis',(1.,0.,0.));
#15123=DIRECTION('',(0.,0.,1.));
#15124=DIRECTION('center_axis',(0.,0.,1.));
#15125=DIRECTION('ref_axis',(1.,0.,0.));
#15126=DIRECTION('center_axis',(0.,0.,1.));
#15127=DIRECTION('ref_axis',(1.,0.,0.));
#15128=DIRECTION('',(0.,0.,1.));
#15129=DIRECTION('center_axis',(1.,0.,0.));
#15130=DIRECTION('ref_axis',(0.,0.,-1.));
#15131=DIRECTION('center_axis',(1.,0.,0.));
#15132=DIRECTION('ref_axis',(0.,0.,-1.));
#15133=DIRECTION('',(1.,0.,0.));
#15134=DIRECTION('center_axis',(-1.,0.,0.));
#15135=DIRECTION('ref_axis',(0.,0.,-1.));
#15136=DIRECTION('center_axis',(0.,1.,0.));
#15137=DIRECTION('ref_axis',(-1.,0.,0.));
#15138=DIRECTION('',(-1.,0.,0.));
#15139=DIRECTION('',(0.,0.,1.));
#15140=DIRECTION('',(-1.,0.,0.));
#15141=DIRECTION('',(0.,0.,1.));
#15142=DIRECTION('center_axis',(1.,0.,0.));
#15143=DIRECTION('ref_axis',(0.,1.,0.));
#15144=DIRECTION('',(0.,1.,0.));
#15145=DIRECTION('',(0.,1.,0.));
#15146=DIRECTION('',(0.,0.,1.));
#15147=DIRECTION('center_axis',(0.,-1.,0.));
#15148=DIRECTION('ref_axis',(1.,0.,0.));
#15149=DIRECTION('',(1.,0.,0.));
#15150=DIRECTION('',(1.,0.,0.));
#15151=DIRECTION('',(0.,0.,1.));
#15152=DIRECTION('center_axis',(-1.,0.,0.));
#15153=DIRECTION('ref_axis',(0.,-1.,0.));
#15154=DIRECTION('',(0.,-1.,0.));
#15155=DIRECTION('',(0.,-1.,0.));
#15156=DIRECTION('center_axis',(0.,0.,1.));
#15157=DIRECTION('ref_axis',(1.,0.,0.));
#15158=DIRECTION('center_axis',(0.,0.,1.));
#15159=DIRECTION('ref_axis',(1.,0.,0.));
#19053=CARTESIAN_POINT('',(0.,0.,0.));
#19054=CARTESIAN_POINT('Origin',(22.25,9.5,0.6));
#19055=CARTESIAN_POINT('',(21.85,9.5,0.6));
#19056=CARTESIAN_POINT('Origin',(22.25,9.5,0.6));
#19057=CARTESIAN_POINT('',(21.85,9.5,6.));
#19058=CARTESIAN_POINT('',(21.85,9.5,0.6));
#19059=CARTESIAN_POINT('Origin',(22.25,9.5,6.));
#19060=CARTESIAN_POINT('Origin',(22.25,9.5,0.6));
#19061=CARTESIAN_POINT('',(22.025,9.5,0.6));
#19062=CARTESIAN_POINT('Origin',(22.25,9.5,0.6));
#19063=CARTESIAN_POINT('Origin',(22.25,12.5,0.6));
#19064=CARTESIAN_POINT('',(21.85,12.5,0.6));
#19065=CARTESIAN_POINT('Origin',(22.25,12.5,0.6));
#19066=CARTESIAN_POINT('',(21.85,12.5,6.));
#19067=CARTESIAN_POINT('',(21.85,12.5,0.6));
#19068=CARTESIAN_POINT('Origin',(22.25,12.5,6.));
#19069=CARTESIAN_POINT('Origin',(22.25,12.5,0.6));
#19070=CARTESIAN_POINT('',(22.025,12.5,0.6));
#19071=CARTESIAN_POINT('Origin',(22.25,12.5,0.6));
#19072=CARTESIAN_POINT('Origin',(22.25,9.5,-0.1));
#19073=CARTESIAN_POINT('',(22.025,9.5,0.));
#19074=CARTESIAN_POINT('Origin',(22.25,9.5,0.));
#19075=CARTESIAN_POINT('',(22.025,9.5,-0.1));
#19076=CARTESIAN_POINT('Origin',(22.25,12.5,-0.1));
#19077=CARTESIAN_POINT('',(22.025,12.5,0.));
#19078=CARTESIAN_POINT('Origin',(22.25,12.5,0.));
#19079=CARTESIAN_POINT('',(22.025,12.5,-0.1));
#19080=CARTESIAN_POINT('Origin',(21.4,11.,4.5));
#19081=CARTESIAN_POINT('',(21.5,11.,5.3));
#19082=CARTESIAN_POINT('Origin',(21.5,11.,4.5));
#19083=CARTESIAN_POINT('',(23.,11.,5.3));
#19084=CARTESIAN_POINT('',(21.4,11.,5.3));
#19085=CARTESIAN_POINT('Origin',(23.,11.,4.5));
#19086=CARTESIAN_POINT('Origin',(23.,13.,0.));
#19087=CARTESIAN_POINT('',(23.,13.,0.));
#19088=CARTESIAN_POINT('',(21.5,13.,0.));
#19089=CARTESIAN_POINT('',(23.,13.,0.));
#19090=CARTESIAN_POINT('',(21.5,13.,6.));
#19091=CARTESIAN_POINT('',(21.5,13.,0.));
#19092=CARTESIAN_POINT('',(23.,13.,6.));
#19093=CARTESIAN_POINT('',(23.,13.,6.));
#19094=CARTESIAN_POINT('',(23.,13.,0.));
#19095=CARTESIAN_POINT('Origin',(23.,9.,0.));
#19096=CARTESIAN_POINT('',(23.,9.,0.));
#19097=CARTESIAN_POINT('',(23.,9.,0.));
#19098=CARTESIAN_POINT('',(23.,9.,6.));
#19099=CARTESIAN_POINT('',(23.,9.,6.));
#19100=CARTESIAN_POINT('',(23.,9.,0.));
#19101=CARTESIAN_POINT('Origin',(21.5,9.,0.));
#19102=CARTESIAN_POINT('',(21.5,9.,0.));
#19103=CARTESIAN_POINT('',(21.5,9.,0.));
#19104=CARTESIAN_POINT('',(21.5,9.,6.));
#19105=CARTESIAN_POINT('',(21.5,9.,6.));
#19106=CARTESIAN_POINT('',(21.5,9.,0.));
#19107=CARTESIAN_POINT('Origin',(21.5,13.,0.));
#19108=CARTESIAN_POINT('',(21.5,13.,0.));
#19109=CARTESIAN_POINT('',(21.5,13.,6.));
#19110=CARTESIAN_POINT('Origin',(22.25,11.,6.));
#19111=CARTESIAN_POINT('Origin',(22.25,11.,0.));
#23469=UNCERTAINTY_MEASURE_WITH_UNIT(LENGTH_MEASURE(0.001),#23588,
'DISTANCE_ACCURACY_VALUE',
'Maximum model space distance between geometric entities at asserted c
onnectivities');
#23522=UNCERTAINTY_MEASURE_WITH_UNIT(LENGTH_MEASURE(0.001),#23588,
'DISTANCE_ACCURACY_VALUE',
'Maximum model space distance between geometric entities at asserted c
onnectivities');
#23534=(
GEOMETRIC_REPRESENTATION_CONTEXT(3)
GLOBAL_UNCERTAINTY_ASSIGNED_CONTEXT((#23469))
GLOBAL_UNIT_ASSIGNED_CONTEXT((#23588,#23590,#23591))
REPRESENTATION_CONTEXT('','3D')
);
#23587=(
GEOMETRIC_REPRESENTATION_CONTEXT(3)
GLOBAL_UNCERTAINTY_ASSIGNED_CONTEXT((#23522))
GLOBAL_UNIT_ASSIGNED_CONTEXT((#23588,#23590,#23591))
REPRESENTATION_CONTEXT('','3D')
);
#23588=(
LENGTH_UNIT()
NAMED_UNIT(*)
SI_UNIT(.CENTI.,.METRE.)
);
#23590=(
NAMED_UNIT(*)
PLANE_ANGLE_UNIT()
SI_UNIT($,.RADIAN.)
);
#23591=(
NAMED_UNIT(*)
SI_UNIT($,.STERADIAN.)
SOLID_ANGLE_UNIT()
);
#23603=SHAPE_DEFINITION_REPRESENTATION(#23667,#23836);
#23667=PRODUCT_DEFINITION_SHAPE('',$,#23901);
#23836=SHAPE_REPRESENTATION('',(#13103),#23534);
#23889=PRODUCT_DEFINITION_CONTEXT('part definition',#24083,'design');
#23901=PRODUCT_DEFINITION('Screw support (1)','Screw support (1)',#23965,
#23889);
#23965=PRODUCT_DEFINITION_FORMATION('',$,#24096);
#24083=APPLICATION_CONTEXT(
'Core Data for Automotive Mechanical Design Process');
#24084=PRODUCT_CONTEXT('part definition',#24083,'mechanical');
#24096=PRODUCT('Screw support (1)','Screw support (1)','Screw support (1)',(#24084));
#24212=COLOUR_RGB('Black',0.12,0.14,0.17);
#24213=FILL_AREA_STYLE_COLOUR('',#24212);
#24214=FILL_AREA_STYLE('',(#24213));
#24215=SURFACE_STYLE_FILL_AREA(#24214);
#24216=SURFACE_SIDE_STYLE('',(#24215));
#24217=SURFACE_STYLE_USAGE(.BOTH.,#24216);
#24218=PRESENTATION_STYLE_ASSIGNMENT((#24217));
ENDSEC;
END-ISO-10303-21;
